ISO-10303-21;
HEADER;
FILE_DESCRIPTION (('STEP AP214'),
    '1' );
FILE_NAME ('Screw 4.step',
    '2026-10-26T17:37:43',
    ( '' ),
    ( '' ),
    'SwSTEP 2.0',
    'SolidWorks 2024',
    '' );
FILE_SCHEMA (( 'AUTOMOTIVE_DESIGN' ));
ENDSEC;

DATA;
#8=VECTOR ( 'NONE', #2227, 1000.000000000000000 ) ;
#66=CARTESIAN_POINT ( 'NONE',  ( 9.987313202991684236, -3657.938829547518253, 2239.009999999999764 ) ) ;
#113=AXIS2_PLACEMENT_3D ( 'NONE', #6268, #9537, #4040 ) ;
#137=FACE_OUTER_BOUND ( 'NONE', #12525, .T. ) ;
#185=VERTEX_POINT ( 'NONE', #21235 ) ;
#187=CARTESIAN_POINT ( 'NONE',  ( 9.987313202740898177, -3661.071170452786646, 2239.009999999999764 ) ) ;
#277=CIRCLE ( 'NONE', #1377, 5.460999999999938126 ) ;
#297=ADVANCED_FACE ( 'NONE', ( #137 ), #12864, .T. ) ;
#303=DIRECTION ( 'NONE',  ( -1.000000000000000000, 1.224646799147353207E-16, 0.000000000000000000 ) ) ;
#376=DIRECTION ( 'NONE',  ( 1.000000000000000000, 5.432398939370943590E-28, -2.324635735433000369E-14 ) ) ;
#407=DIRECTION ( 'NONE',  ( 0.000000000000000000, 1.000000000000000000, 0.000000000000000000 ) ) ;
#424=VERTEX_POINT ( 'NONE', #18285 ) ;
#430=CARTESIAN_POINT ( 'NONE',  ( 12.69999999999999929, -3659.504999999999654, 2239.391000000000076 ) ) ;
#443=CARTESIAN_POINT ( 'NONE',  ( 10.36831320285999958, -3658.158799999999701, 2242.820000000000164 ) ) ;
#463=DIRECTION ( 'NONE',  ( -0.8660254037840939834, -0.5000000000005969669, 0.000000000000000000 ) ) ;
#481=ORIENTED_EDGE ( 'NONE', *, *, #20058, .F. ) ;
#483=APPLICATION_CONTEXT ( 'configuration controlled 3d designs of mechanical parts and assemblies' ) ;
#603=CARTESIAN_POINT ( 'NONE',  ( 12.69999999999999929, -3659.504999999999654, 2245.359999999999673 ) ) ;
#611=AXIS2_PLACEMENT_3D ( 'NONE', #16670, #22278, #6258 ) ;
#643=TOROIDAL_SURFACE ( 'NONE', #13371, 5.080000000000000071, 0.3810000000000000053 ) ;
#644=DIRECTION ( 'NONE',  ( 0.8660254037825932949, 0.5000000000031962211, 0.000000000000000000 ) ) ;
#672=( BOUNDED_CURVE ( )  B_SPLINE_CURVE ( 3, ( #2113, #7152, #5395, #8907 ),
 .UNSPECIFIED., .F., .T. ) 
 B_SPLINE_CURVE_WITH_KNOTS ( ( 4, 4 ),
 ( 1.570796326475431659, 3.141592653589783346 ),
 .UNSPECIFIED. ) 
 CURVE ( )  GEOMETRIC_REPRESENTATION_ITEM ( )  RATIONAL_B_SPLINE_CURVE ( ( 1.000000000000000000, 0.8047378540490687238, 0.8047378540490687238, 1.000000000000000000 ) ) 
 REPRESENTATION_ITEM ( '' )  );
#709=ORIENTED_EDGE ( 'NONE', *, *, #3573, .F. ) ;
#796=VERTEX_POINT ( 'NONE', #19151 ) ;
#845=DIRECTION ( 'NONE',  ( 0.8660254037821217832, -0.5000000000040129011, 0.000000000000000000 ) ) ;
#888=DIRECTION ( 'NONE',  ( 0.000000000000000000, 0.000000000000000000, -1.000000000000000000 ) ) ;
#902=EDGE_CURVE ( 'NONE', #6944, #20781, #3036, .T. ) ;
#909=VECTOR ( 'NONE', #12471, 1000.000000000000000 ) ;
#976=ADVANCED_FACE ( 'NONE', ( #7198 ), #21945, .T. ) ;
#984=CARTESIAN_POINT ( 'NONE',  ( 12.70000000005999929, -3656.812599999999748, 2242.820000000000164 ) ) ;
#1024=FACE_OUTER_BOUND ( 'NONE', #8988, .T. ) ;
#1090=DIRECTION ( 'NONE',  ( 2.324635735433000053E-14, 0.000000000000000000, 1.000000000000000000 ) ) ;
#1182=VECTOR ( 'NONE', #22756, 1000.000000000000000 ) ;
#1189=DIRECTION ( 'NONE',  ( -0.8660254037842058938, -0.5000000000004030110, 0.000000000000000000 ) ) ;
#1212=CARTESIAN_POINT ( 'NONE',  ( 12.70000000002640839, -3656.812599999929262, 2239.391000000000076 ) ) ;
#1220=VECTOR ( 'NONE', #22541, 1000.000000000000000 ) ;
#1248=LINE ( 'NONE', #9918, #11318 ) ;
#1377=AXIS2_PLACEMENT_3D ( 'NONE', #15369, #15259, #22498 ) ;
#1430=( NAMED_UNIT ( * ) PLANE_ANGLE_UNIT ( ) SI_UNIT ( $, .RADIAN. ) );
#1441=ORIENTED_EDGE ( 'NONE', *, *, #10538, .T. ) ;
#1442=ORIENTED_EDGE ( 'NONE', *, *, #6454, .F. ) ;
#1469=FACE_OUTER_BOUND ( 'NONE', #5404, .T. ) ;
#1535=CARTESIAN_POINT ( 'NONE',  ( 12.70000000002425899, -3662.197400000083690, 2239.391000000000076 ) ) ;
#1539=CARTESIAN_POINT ( 'NONE',  ( 12.69999999999999929, -3659.504999999999654, 2245.359999999999673 ) ) ;
#1570=CARTESIAN_POINT ( 'NONE',  ( 15.03168679717000167, -3660.851200000000063, 2242.820000000000164 ) ) ;
#1669=AXIS2_PLACEMENT_3D ( 'NONE', #19032, #13877, #15867 ) ;
#1674=APPLICATION_CONTEXT ( 'configuration controlled 3d designs of mechanical parts and assemblies' ) ;
#1688=DIRECTION ( 'NONE',  ( 0.000000000000000000, 0.000000000000000000, -1.000000000000000000 ) ) ;
#1757=ORIENTED_EDGE ( 'NONE', *, *, #5135, .T. ) ;
#1763=DIRECTION ( 'NONE',  ( 0.8660254037841628172, 0.5000000000004778400, -5.443078266502769467E-12 ) ) ;
#1765=VECTOR ( 'NONE', #1189, 1000.000000000000114 ) ;
#1815=PRODUCT_CONTEXT ( 'NONE', #483, 'mechanical' ) ;
#1844=DIRECTION ( 'NONE',  ( 0.000000000000000000, 0.000000000000000000, -1.000000000000000000 ) ) ;
#1849=CARTESIAN_POINT ( 'NONE',  ( 12.69999999999999929, -3664.965999999999894, 2239.391000000000076 ) ) ;
#1937=DIRECTION ( 'NONE',  ( 0.000000000000000000, -1.000000000000000000, 0.000000000000000000 ) ) ;
#1981=DIRECTION ( 'NONE',  ( 0.000000000000000000, 0.000000000000000000, -1.000000000000000000 ) ) ;
#2013=PLANE ( 'NONE',  #2455 ) ;
#2018=CARTESIAN_POINT ( 'NONE',  ( 10.36831320292846925, -3660.851200000039626, 2239.391000000000076 ) ) ;
#2071=FACE_OUTER_BOUND ( 'NONE', #20364, .T. ) ;
#2084=EDGE_CURVE ( 'NONE', #796, #185, #1248, .T. ) ;
#2113=CARTESIAN_POINT ( 'NONE',  ( 15.41268679728733915, -3657.938829547220848, 2239.009999999999764 ) ) ;
#2133=DIRECTION ( 'NONE',  ( 0.000000000000000000, -1.000000000000000000, 4.457650181899999573E-12 ) ) ;
#2227=DIRECTION ( 'NONE',  ( 0.000000000000000000, 0.000000000000000000, -1.000000000000000000 ) ) ;
#2247=LINE ( 'NONE', #19947, #8695 ) ;
#2249=CARTESIAN_POINT ( 'NONE',  ( 10.21049783553369217, -3660.942314744965188, 2239.009999999927913 ) ) ;
#2257=( GEOMETRIC_REPRESENTATION_CONTEXT ( 3 ) GLOBAL_UNCERTAINTY_ASSIGNED_CONTEXT ( ( #16741 ) ) GLOBAL_UNIT_ASSIGNED_CONTEXT ( ( #21126, #3419, #23094 ) ) REPRESENTATION_CONTEXT ( 'NONE', 'WORKASPACE' ) );
#2258=EDGE_CURVE ( 'NONE', #16093, #13523, #15074, .T. ) ;
#2278=AXIS2_PLACEMENT_3D ( 'NONE', #10800, #7514, #5774 ) ;
#2300=EDGE_CURVE ( 'NONE', #10412, #16994, #3198, .T. ) ;
#2308=ORIENTED_EDGE ( 'NONE', *, *, #12141, .T. ) ;
#2312=CARTESIAN_POINT ( 'NONE',  ( 15.41268679715999923, -3657.938829547000296, 2239.009999999999764 ) ) ;
#2325=CARTESIAN_POINT ( 'NONE',  ( 12.69999999999999929, -3659.504999999999654, 2270.760000000000218 ) ) ;
#2355=ADVANCED_FACE ( 'NONE', ( #16813 ), #9107, .T. ) ;
#2374=ADVANCED_BREP_SHAPE_REPRESENTATION ( '', ( #21208, #5611 ), #14603 ) ;
#2376=DIRECTION ( 'NONE',  ( 0.000000000000000000, -1.000000000000000000, 0.000000000000000000 ) ) ;
#2455=AXIS2_PLACEMENT_3D ( 'NONE', #21588, #17937, #2133 ) ;
#2479=CIRCLE ( 'NONE', #4709, 0.3809999999999647002 ) ;
#2517=ORIENTED_EDGE ( 'NONE', *, *, #20569, .F. ) ;
#2519=FACE_OUTER_BOUND ( 'NONE', #15863, .T. ) ;
#2538=FACE_OUTER_BOUND ( 'NONE', #15528, .T. ) ;
#2561=DIRECTION ( 'NONE',  ( 0.000000000000000000, 0.000000000000000000, -1.000000000000000000 ) ) ;
#2606=CARTESIAN_POINT ( 'NONE',  ( 0.000000000000000000, 0.000000000000000000, 0.000000000000000000 ) ) ;
#2610=LINE ( 'NONE', #16900, #19347 ) ;
#2700=CARTESIAN_POINT ( 'NONE',  ( 7.619999999999999218, -3659.504999999999654, 2245.359999999999673 ) ) ;
#2777=VERTEX_POINT ( 'NONE', #11485 ) ;
#2794=CARTESIAN_POINT ( 'NONE',  ( 7.619999999999999218, -3659.504999999999654, 2239.391000000000076 ) ) ;
#2829=DIRECTION ( 'NONE',  ( -2.848935406719999894E-12, 1.000000000000000000, 2.336881798978000141E-14 ) ) ;
#2843=VECTOR ( 'NONE', #21075, 1000.000000000000000 ) ;
#2845=DIRECTION ( 'NONE',  ( 5.432398939370942693E-28, 1.000000000000000000, 2.336881798971000105E-14 ) ) ;
#2893=CARTESIAN_POINT ( 'NONE',  ( 15.03168679716000078, -3658.158799999999701, 2239.391000000000076 ) ) ;
#2903=AXIS2_PLACEMENT_3D ( 'NONE', #11080, #14834, #20111 ) ;
#2980=DIRECTION ( 'NONE',  ( -2.324635735433000053E-14, 0.000000000000000000, -1.000000000000000000 ) ) ;
#2997=CARTESIAN_POINT ( 'NONE',  ( 14.05634339859000015, -3657.155744320999929, 2239.391000000000076 ) ) ;
#3007=DIRECTION ( 'NONE',  ( 2.150065550568999996E-13, 0.000000000000000000, -1.000000000000000000 ) ) ;
#3036=CIRCLE ( 'NONE', #8649, 5.460999999999938126 ) ;
#3119=ORIENTED_EDGE ( 'NONE', *, *, #20383, .F. ) ;
#3175=FACE_OUTER_BOUND ( 'NONE', #5544, .T. ) ;
#3194=PRODUCT ( 'Screw 4', 'Screw 4', '', ( #1815 ) ) ;
#3198=( BOUNDED_CURVE ( )  B_SPLINE_CURVE ( 3, ( #16474, #9560, #4713, #21979 ),
 .UNSPECIFIED., .F., .T. ) 
 B_SPLINE_CURVE_WITH_KNOTS ( ( 4, 4 ),
 ( -2.664535259100375697E-14, 1.570796326276726607 ),
 .UNSPECIFIED. ) 
 CURVE ( )  GEOMETRIC_REPRESENTATION_ITEM ( )  RATIONAL_B_SPLINE_CURVE ( ( 1.000000000000000000, 0.8047378542464924678, 0.8047378542464924678, 1.000000000000000000 ) ) 
 REPRESENTATION_ITEM ( '' )  );
#3261=EDGE_CURVE ( 'NONE', #20781, #20823, #17078, .T. ) ;
#3274=EDGE_LOOP ( 'NONE', ( #2308, #13362 ) ) ;
#3325=CARTESIAN_POINT ( 'NONE',  ( 7.619999999999999218, -3659.504999999999654, 2244.978999999999814 ) ) ;
#3419=( NAMED_UNIT ( * ) PLANE_ANGLE_UNIT ( ) SI_UNIT ( $, .RADIAN. ) );
#3421=AXIS2_PLACEMENT_3D ( 'NONE', #19781, #14509, #1844 ) ;
#3434=ORIENTED_EDGE ( 'NONE', *, *, #8730, .F. ) ;
#3551=ORIENTED_EDGE ( 'NONE', *, *, #8136, .T. ) ;
#3573=EDGE_CURVE ( 'NONE', #8067, #20661, #18227, .T. ) ;
#3581=CIRCLE ( 'NONE', #22655, 5.460999999999938126 ) ;
#3583=CIRCLE ( 'NONE', #7341, 0.3809999999999647002 ) ;
#3589=FACE_OUTER_BOUND ( 'NONE', #3274, .T. ) ;
#3600=AXIS2_PLACEMENT_3D ( 'NONE', #2794, #8079, #13462 ) ;
#3664=ORIENTED_EDGE ( 'NONE', *, *, #2084, .F. ) ;
#3740=LINE ( 'NONE', #3864, #7779 ) ;
#3781=ORIENTED_EDGE ( 'NONE', *, *, #15978, .F. ) ;
#3783=DIRECTION ( 'NONE',  ( 2.324635735433000053E-14, 0.000000000000000000, 1.000000000000000000 ) ) ;
#3810=CARTESIAN_POINT ( 'NONE',  ( 12.69999999999999929, -3661.409999999999400, 2272.030000000000200 ) ) ;
#3864=CARTESIAN_POINT ( 'NONE',  ( 10.36831320285999958, -3658.158799999999701, 2242.820000000000164 ) ) ;
#3881=ORIENTED_EDGE ( 'NONE', *, *, #16999, .F. ) ;
#3918=VERTEX_POINT ( 'NONE', #2700 ) ;
#3948=CARTESIAN_POINT ( 'NONE',  ( 17.78000000000000114, -3659.504999999999654, 2239.009999999999764 ) ) ;
#3992=DIRECTION ( 'NONE',  ( 0.000000000000000000, -2.336881798971000105E-14, 1.000000000000000000 ) ) ;
#4023=ORIENTED_EDGE ( 'NONE', *, *, #10946, .F. ) ;
#4040=DIRECTION ( 'NONE',  ( 0.000000000000000000, -1.000000000000000000, 0.000000000000000000 ) ) ;
#4041=AXIS2_PLACEMENT_3D ( 'NONE', #11345, #9596, #9480 ) ;
#4064=CARTESIAN_POINT ( 'NONE',  ( 12.69999999999999929, -3657.599999999999909, 2272.030000000000200 ) ) ;
#4080=DIRECTION ( 'NONE',  ( 0.5000000000005969669, -0.8660254037840939834, 0.000000000000000000 ) ) ;
#4135=ORIENTED_EDGE ( 'NONE', *, *, #21053, .F. ) ;
#4137=DIRECTION ( 'NONE',  ( 0.000000000000000000, 0.000000000000000000, -1.000000000000000000 ) ) ;
#4189=FACE_OUTER_BOUND ( 'NONE', #19073, .T. ) ;
#4202=ORIENTED_EDGE ( 'NONE', *, *, #3573, .T. ) ;
#4218=ORIENTED_EDGE ( 'NONE', *, *, #8730, .T. ) ;
#4261=DIRECTION ( 'NONE',  ( -0.5000000000043351989, -0.8660254037819355988, 0.000000000000000000 ) ) ;
#4278=EDGE_CURVE ( 'NONE', #13523, #8067, #18384, .T. ) ;
#4293=EDGE_CURVE ( 'NONE', #20781, #10638, #21906, .T. ) ;
#4331=ORIENTED_EDGE ( 'NONE', *, *, #3261, .T. ) ;
#4362=ORIENTED_EDGE ( 'NONE', *, *, #2300, .F. ) ;
#4424=DIRECTION ( 'NONE',  ( -0.8660254037815640071, 0.5000000000049790172, 0.000000000000000000 ) ) ;
#4480=ADVANCED_FACE ( 'NONE', ( #1024 ), #18842, .T. ) ;
#4517=CARTESIAN_POINT ( 'NONE',  ( 10.36831320285999958, -3658.158799999999701, 2239.391000000000076 ) ) ;
#4538=ORIENTED_EDGE ( 'NONE', *, *, #9152, .F. ) ;
#4705=( BOUNDED_CURVE ( )  B_SPLINE_CURVE ( 3, ( #5482, #12622, #9105, #16245 ),
 .UNSPECIFIED., .F., .T. ) 
 B_SPLINE_CURVE_WITH_KNOTS ( ( 4, 4 ),
 ( 1.570796327116351643, 3.141592653589766471 ),
 .UNSPECIFIED. ) 
 CURVE ( )  GEOMETRIC_REPRESENTATION_ITEM ( )  RATIONAL_B_SPLINE_CURVE ( ( 1.000000000000000000, 0.8047378542001389912, 0.8047378542001389912, 1.000000000000000000 ) ) 
 REPRESENTATION_ITEM ( '' )  );
#4709=AXIS2_PLACEMENT_3D ( 'NONE', #19019, #2845, #17599 ) ;
#4711=DIRECTION ( 'NONE',  ( -1.000000000000000000, 0.000000000000000000, 2.324635735433000053E-14 ) ) ;
#4713=CARTESIAN_POINT ( 'NONE',  ( 10.21049783570185099, -3658.067685255140532, 2239.010000000115724 ) ) ;
#4719=LINE ( 'NONE', #8819, #1765 ) ;
#4819=EDGE_LOOP ( 'NONE', ( #11129, #7442 ) ) ;
#4837=EDGE_CURVE ( 'NONE', #10412, #2777, #12019, .T. ) ;
#4888=ORIENTED_EDGE ( 'NONE', *, *, #18548, .T. ) ;
#4891=EDGE_LOOP ( 'NONE', ( #9834, #5824, #9607, #3434 ) ) ;
#4949=FACE_OUTER_BOUND ( 'NONE', #11379, .T. ) ;
#4962=AXIS2_PLACEMENT_3D ( 'NONE', #12501, #19651, #12733 ) ;
#4968=ORIENTED_EDGE ( 'NONE', *, *, #2258, .T. ) ;
#4973=ADVANCED_FACE ( 'NONE', ( #2538 ), #9786, .T. ) ;
#5009=LINE ( 'NONE', #22915, #21662 ) ;
#5074=PLANE ( 'NONE',  #18946 ) ;
#5087=VERTEX_POINT ( 'NONE', #19631 ) ;
#5101=AXIS2_PLACEMENT_3D ( 'NONE', #18043, #463, #14765 ) ;
#5135=EDGE_CURVE ( 'NONE', #16093, #11557, #15699, .T. ) ;
#5156=ADVANCED_FACE ( 'NONE', ( #14936 ), #5930, .T. ) ;
#5184=DIRECTION ( 'NONE',  ( 1.000000000000000000, 2.331176954593497545E-12, 0.000000000000000000 ) ) ;
#5207=LINE ( 'NONE', #12113, #19703 ) ;
#5222=CARTESIAN_POINT ( 'NONE',  ( 15.03168679717000167, -3660.851200000000063, 2242.820000000000164 ) ) ;
#5247=ORIENTED_EDGE ( 'NONE', *, *, #4837, .F. ) ;
#5327=CARTESIAN_POINT ( 'NONE',  ( 12.69999999999999929, -3659.504999999999654, 2270.760000000000218 ) ) ;
#5333=DIRECTION ( 'NONE',  ( -1.990254351990999514E-12, 1.000000000000000000, -3.793660610075000646E-12 ) ) ;
#5368=CARTESIAN_POINT ( 'NONE',  ( 10.36831320285999958, -3658.158799999999701, 2242.820000000000164 ) ) ;
#5384=CARTESIAN_POINT ( 'NONE',  ( 17.78000000000000114, -3659.504999999999654, 2245.359999999999673 ) ) ;
#5395=CARTESIAN_POINT ( 'NONE',  ( 15.03168679716618961, -3658.158799999851908, 2239.167815367207822 ) ) ;
#5404=EDGE_LOOP ( 'NONE', ( #1442, #22657, #9218, #22162 ) ) ;
#5420=PLANE ( 'NONE',  #2278 ) ;
#5441=EDGE_LOOP ( 'NONE', ( #12405, #18082, #3119, #12208 ) ) ;
#5448=VERTEX_POINT ( 'NONE', #16174 ) ;
#5471=VECTOR ( 'NONE', #11791, 1000.000000000000000 ) ;
#5482=CARTESIAN_POINT ( 'NONE',  ( 15.41268679705191857, -3661.071170452636579, 2239.009999999999764 ) ) ;
#5493=DIRECTION ( 'NONE',  ( -2.170301461641000033E-13, 1.295098308111999954E-13, -1.000000000000000000 ) ) ;
#5510=AXIS2_PLACEMENT_3D ( 'NONE', #13502, #13161, #4261 ) ;
#5525=EDGE_CURVE ( 'NONE', #5448, #12925, #3740, .T. ) ;
#5544=EDGE_LOOP ( 'NONE', ( #13828, #14208, #18868, #18201 ) ) ;
#5549=DIRECTION ( 'NONE',  ( -0.8660254037839142383, -0.5000000000009082735, 0.000000000000000000 ) ) ;
#5594=LINE ( 'NONE', #17998, #11081 ) ;
#5611=AXIS2_PLACEMENT_3D ( 'NONE', #2606, #9751, #7545 ) ;
#5711=DIRECTION ( 'NONE',  ( 0.8660254037826368156, 0.5000000000031208369, 0.000000000000000000 ) ) ;
#5749=ORIENTED_EDGE ( 'NONE', *, *, #18697, .T. ) ;
#5763=CARTESIAN_POINT ( 'NONE',  ( 12.69999999999999929, -3659.504999999999654, 2245.359999999999673 ) ) ;
#5774=DIRECTION ( 'NONE',  ( -0.8660254037817187722, 0.5000000000047108983, 0.000000000000000000 ) ) ;
#5819=DIRECTION ( 'NONE',  ( -2.324635735433000053E-14, 2.336881798971000105E-14, -1.000000000000000000 ) ) ;
#5824=ORIENTED_EDGE ( 'NONE', *, *, #21053, .T. ) ;
#5887=ORIENTED_EDGE ( 'NONE', *, *, #15425, .F. ) ;
#5911=CARTESIAN_POINT ( 'NONE',  ( 10.36831320285999958, -3660.851200000000063, 2242.820000000000164 ) ) ;
#5930=TOROIDAL_SURFACE ( 'NONE', #8161, 1.905000000000000027, 1.270000000000000018 ) ;
#5972=PRODUCT_DEFINITION_CONTEXT ( 'detailed design', #1674, 'design' ) ;
#6017=AXIS2_PLACEMENT_3D ( 'NONE', #8186, #16963, #12045 ) ;
#6020=ORIENTED_EDGE ( 'NONE', *, *, #13208, .T. ) ;
#6030=CYLINDRICAL_SURFACE ( 'NONE', #5510, 0.3809999999998115450 ) ;
#6038=DIRECTION ( 'NONE',  ( -0.8660254037816071948, 0.5000000000049040771, 0.000000000000000000 ) ) ;
#6090=( BOUNDED_CURVE ( )  B_SPLINE_CURVE ( 3, ( #13319, #13092, #15311, #16939 ),
 .UNSPECIFIED., .F., .T. ) 
 B_SPLINE_CURVE_WITH_KNOTS ( ( 4, 4 ),
 ( 1.570796327146205540, 3.141592653589829531 ),
 .UNSPECIFIED. ) 
 CURVE ( )  GEOMETRIC_REPRESENTATION_ITEM ( )  RATIONAL_B_SPLINE_CURVE ( ( 1.000000000000000000, 0.8047378542071605967, 0.8047378542071605967, 1.000000000000000000 ) ) 
 REPRESENTATION_ITEM ( '' )  );
#6120=DIRECTION ( 'NONE',  ( -1.000000000000000000, 0.000000000000000000, 0.000000000000000000 ) ) ;
#6173=AXIS2_PLACEMENT_3D ( 'NONE', #22535, #6630, #17267 ) ;
#6258=DIRECTION ( 'NONE',  ( 0.000000000000000000, -1.000000000000000000, 0.000000000000000000 ) ) ;
#6268=CARTESIAN_POINT ( 'NONE',  ( 12.69999999999999929, -3659.504999999999654, 2239.391000000000076 ) ) ;
#6311=DIRECTION ( 'NONE',  ( 0.000000000000000000, -1.000000000000000000, 0.000000000000000000 ) ) ;
#6313=CARTESIAN_POINT ( 'NONE',  ( 12.69999999999999929, -3659.504999999999654, 2239.009999999999764 ) ) ;
#6360=ORIENTED_EDGE ( 'NONE', *, *, #10495, .F. ) ;
#6366=VECTOR ( 'NONE', #2561, 1000.000000000000000 ) ;
#6453=VECTOR ( 'NONE', #7129, 1000.000000000000000 ) ;
#6454=EDGE_CURVE ( 'NONE', #13782, #13805, #9660, .T. ) ;
#6588=AXIS2_PLACEMENT_3D ( 'NONE', #13796, #21184, #10505 ) ;
#6630=DIRECTION ( 'NONE',  ( 5.432398939370942693E-28, 1.000000000000000000, 2.336881798971000105E-14 ) ) ;
#6632=CYLINDRICAL_SURFACE ( 'NONE', #10710, 3.175000000000149925 ) ;
#6647=DIRECTION ( 'NONE',  ( 1.278298683860999806E-12, -1.000000000000000000, 0.000000000000000000 ) ) ;
#6689=ORIENTED_EDGE ( 'NONE', *, *, #3261, .F. ) ;
#6710=VECTOR ( 'NONE', #20943, 1000.000000000000000 ) ;
#6720=DIRECTION ( 'NONE',  ( 1.000000000000000000, 5.432398939370943590E-28, -2.324635735433000369E-14 ) ) ;
#6736=DIRECTION ( 'NONE',  ( 0.8660254037827048723, 0.5000000000030029312, 0.000000000000000000 ) ) ;
#6832=EDGE_CURVE ( 'NONE', #16601, #9582, #277, .T. ) ;
#6841=FACE_OUTER_BOUND ( 'NONE', #5441, .T. ) ;
#6909=DIRECTION ( 'NONE',  ( -3.106212348370000105E-13, -6.475491540576999783E-13, 1.000000000000000000 ) ) ;
#6931=ADVANCED_FACE ( 'NONE', ( #11384 ), #20518, .T. ) ;
#6944=VERTEX_POINT ( 'NONE', #7993 ) ;
#6997=DIRECTION ( 'NONE',  ( 0.5000000000048030468, 0.8660254037816655925, 0.000000000000000000 ) ) ;
#7063=EDGE_LOOP ( 'NONE', ( #21649, #22784, #10417, #7369, #15537, #3881 ) ) ;
#7075=CARTESIAN_POINT ( 'NONE',  ( 7.238999999999998991, -3659.504999999999654, 2239.391000000000531 ) ) ;
#7099=ORIENTED_EDGE ( 'NONE', *, *, #15978, .T. ) ;
#7129=DIRECTION ( 'NONE',  ( 1.736749921369999674E-12, -1.000000000000000000, 0.000000000000000000 ) ) ;
#7135=ORIENTED_EDGE ( 'NONE', *, *, #14104, .F. ) ;
#7152=CARTESIAN_POINT ( 'NONE',  ( 15.18950216449525925, -3658.067685255041397, 2239.009999999928368 ) ) ;
#7170=DIRECTION ( 'NONE',  ( 0.000000000000000000, 0.000000000000000000, 1.000000000000000000 ) ) ;
#7173=CARTESIAN_POINT ( 'NONE',  ( 12.70000000028313281, -3656.372659094870869, 2239.009999999999764 ) ) ;
#7198=FACE_OUTER_BOUND ( 'NONE', #16069, .T. ) ;
#7281=ADVANCED_FACE ( 'NONE', ( #6841 ), #5074, .T. ) ;
#7303=EDGE_CURVE ( 'NONE', #22029, #9475, #2479, .T. ) ;
#7341=AXIS2_PLACEMENT_3D ( 'NONE', #3325, #20793, #1688 ) ;
#7343=ORIENTED_EDGE ( 'NONE', *, *, #2258, .F. ) ;
#7369=ORIENTED_EDGE ( 'NONE', *, *, #20058, .T. ) ;
#7406=CIRCLE ( 'NONE', #4041, 5.080000000000000959 ) ;
#7411=CARTESIAN_POINT ( 'NONE',  ( 12.69999999999999929, -3659.504999999999654, 2244.978999999999814 ) ) ;
#7442=ORIENTED_EDGE ( 'NONE', *, *, #9152, .T. ) ;
#7478=LINE ( 'NONE', #13553, #5471 ) ;
#7503=DIRECTION ( 'NONE',  ( -1.000000000000000000, 0.000000000000000000, 0.000000000000000000 ) ) ;
#7507=CARTESIAN_POINT ( 'NONE',  ( 12.69999999999999929, -3659.504999999999654, 2270.760000000000218 ) ) ;
#7514=DIRECTION ( 'NONE',  ( -0.5000000000047110094, -0.8660254037817188832, 0.000000000000000000 ) ) ;
#7545=DIRECTION ( 'NONE',  ( 1.000000000000000000, 0.000000000000000000, 0.000000000000000000 ) ) ;
#7582=CIRCLE ( 'NONE', #113, 5.460999999999938126 ) ;
#7585=ADVANCED_FACE ( 'NONE', ( #14445 ), #5420, .T. ) ;
#7666=CARTESIAN_POINT ( 'NONE',  ( 12.69999999999999929, -3659.504999999999654, 2270.760000000000218 ) ) ;
#7680=DIRECTION ( 'NONE',  ( 1.000000000000000000, 1.206643234470999950E-12, 0.000000000000000000 ) ) ;
#7704=ORIENTED_EDGE ( 'NONE', *, *, #21194, .F. ) ;
#7724=AXIS2_PLACEMENT_3D ( 'NONE', #11893, #2980, #13774 ) ;
#7779=VECTOR ( 'NONE', #1763, 999.9999999999998863 ) ;
#7793=DIRECTION ( 'NONE',  ( 0.5000000000031612490, -0.8660254037826135010, 0.000000000000000000 ) ) ;
#7813=EDGE_CURVE ( 'NONE', #20661, #8067, #10987, .T. ) ;
#7850=LINE ( 'NONE', #13349, #11846 ) ;
#7909=CARTESIAN_POINT ( 'NONE',  ( 9.987313202862001305, -3659.504999999999654, 2239.391000000000076 ) ) ;
#7993=CARTESIAN_POINT ( 'NONE',  ( 18.16100000000000136, -3659.504999999999654, 2244.978999999999814 ) ) ;
#8067=VERTEX_POINT ( 'NONE', #10247 ) ;
#8079=DIRECTION ( 'NONE',  ( 1.224646799141920914E-16, -1.000000000000000000, -2.336881798971000421E-14 ) ) ;
#8136=EDGE_CURVE ( 'NONE', #21944, #15061, #19279, .T. ) ;
#8138=( BOUNDED_CURVE ( )  B_SPLINE_CURVE ( 3, ( #2018, #14563, #2249, #9402 ),
 .UNSPECIFIED., .F., .F. ) 
 B_SPLINE_CURVE_WITH_KNOTS ( ( 4, 4 ),
 ( -9.769962616701377556E-15, 1.570796327117804925 ),
 .UNSPECIFIED. ) 
 CURVE ( )  GEOMETRIC_REPRESENTATION_ITEM ( )  RATIONAL_B_SPLINE_CURVE ( ( 1.000000000000000000, 0.8047378540482524878, 0.8047378540482524878, 1.000000000000000000 ) ) 
 REPRESENTATION_ITEM ( '' )  );
#8161=AXIS2_PLACEMENT_3D ( 'NONE', #7666, #21959, #407 ) ;
#8186=CARTESIAN_POINT ( 'NONE',  ( 12.69999999999999929, -3659.504999999999654, 2245.359999999999673 ) ) ;
#8283=ORIENTED_EDGE ( 'NONE', *, *, #19549, .F. ) ;
#8372=ORIENTED_EDGE ( 'NONE', *, *, #4278, .T. ) ;
#8382=DIRECTION ( 'NONE',  ( -0.8660254037821217832, 0.5000000000040129011, 1.814359422183044529E-12 ) ) ;
#8416=ADVANCED_FACE ( 'NONE', ( #22061 ), #6030, .T. ) ;
#8425=AXIS2_PLACEMENT_3D ( 'NONE', #21436, #12298, #15582 ) ;
#8437=EDGE_CURVE ( 'NONE', #19095, #13134, #2610, .T. ) ;
#8479=EDGE_LOOP ( 'NONE', ( #19302, #9203 ) ) ;
#8570=EDGE_CURVE ( 'NONE', #13091, #10412, #4719, .T. ) ;
#8617=ORIENTED_EDGE ( 'NONE', *, *, #22408, .T. ) ;
#8649=AXIS2_PLACEMENT_3D ( 'NONE', #9070, #3783, #9309 ) ;
#8676=ADVANCED_FACE ( 'NONE', ( #12910 ), #643, .T. ) ;
#8695=VECTOR ( 'NONE', #5549, 1000.000000000000114 ) ;
#8696=FACE_BOUND ( 'NONE', #20678, .T. ) ;
#8730=EDGE_CURVE ( 'NONE', #2777, #19095, #8138, .T. ) ;
#8762=CARTESIAN_POINT ( 'NONE',  ( 12.69999999999999929, -3659.504999999999654, 2245.359999999999673 ) ) ;
#8769=CARTESIAN_POINT ( 'NONE',  ( 10.36831320293767078, -3658.158799999985604, 2239.391000000000076 ) ) ;
#8781=EDGE_CURVE ( 'NONE', #19866, #3918, #13012, .T. ) ;
#8782=EDGE_LOOP ( 'NONE', ( #15550, #1757, #14406, #5887 ) ) ;
#8813=ORIENTED_EDGE ( 'NONE', *, *, #7813, .T. ) ;
#8819=CARTESIAN_POINT ( 'NONE',  ( 12.70000000005999929, -3656.812599999999748, 2239.391000000000076 ) ) ;
#8907=CARTESIAN_POINT ( 'NONE',  ( 15.03168679710029743, -3658.158799999889197, 2239.391000000000076 ) ) ;
#8981=CARTESIAN_POINT ( 'NONE',  ( 10.36831320285999958, -3658.158799999999701, 2242.820000000000164 ) ) ;
#8988=EDGE_LOOP ( 'NONE', ( #6689, #20652, #11565, #20387, #481, #13898 ) ) ;
#9010=EDGE_CURVE ( 'NONE', #13782, #185, #672, .T. ) ;
#9070=CARTESIAN_POINT ( 'NONE',  ( 12.69999999999999929, -3659.504999999999654, 2244.978999999999814 ) ) ;
#9102=PLANE ( 'NONE',  #11752 ) ;
#9105=CARTESIAN_POINT ( 'NONE',  ( 15.03168679717383682, -3660.851200000147401, 2239.167815367321055 ) ) ;
#9107=TOROIDAL_SURFACE ( 'NONE', #11331, 5.080000000000000071, 0.3810000000000000053 ) ;
#9152=EDGE_CURVE ( 'NONE', #15597, #9475, #7406, .T. ) ;
#9169=DIRECTION ( 'NONE',  ( -2.324635735433000053E-14, 2.336881798971000105E-14, -1.000000000000000000 ) ) ;
#9179=ORIENTED_EDGE ( 'NONE', *, *, #10946, .T. ) ;
#9203=ORIENTED_EDGE ( 'NONE', *, *, #19549, .T. ) ;
#9206=CARTESIAN_POINT ( 'NONE',  ( 12.69999999999999929, -3661.409999999999400, 2270.760000000000218 ) ) ;
#9215=PRODUCT_DEFINITION_SHAPE ( 'NONE', 'NONE',  #20962 ) ;
#9218=ORIENTED_EDGE ( 'NONE', *, *, #12530, .T. ) ;
#9300=EDGE_CURVE ( 'NONE', #5448, #10412, #17898, .T. ) ;
#9309=DIRECTION ( 'NONE',  ( 0.000000000000000000, -1.000000000000000000, 0.000000000000000000 ) ) ;
#9327=FACE_OUTER_BOUND ( 'NONE', #13169, .T. ) ;
#9346=VECTOR ( 'NONE', #6647, 1000.000000000000000 ) ;
#9358=CARTESIAN_POINT ( 'NONE',  ( 12.70000000005999929, -3656.812599999999748, 2242.820000000000164 ) ) ;
#9361=VERTEX_POINT ( 'NONE', #17776 ) ;
#9402=CARTESIAN_POINT ( 'NONE',  ( 9.987313202740898177, -3661.071170452786646, 2239.009999999999764 ) ) ;
#9434=ORIENTED_EDGE ( 'NONE', *, *, #5135, .F. ) ;
#9442=DIRECTION ( 'NONE',  ( -0.8660254037825932949, -0.5000000000031962211, 5.608020032303961777E-12 ) ) ;
#9475=VERTEX_POINT ( 'NONE', #3948 ) ;
#9480=DIRECTION ( 'NONE',  ( 1.000000000000000000, 0.000000000000000000, 0.000000000000000000 ) ) ;
#9536=AXIS2_PLACEMENT_3D ( 'NONE', #5763, #3992, #7503 ) ;
#9537=DIRECTION ( 'NONE',  ( -2.324635735433000053E-14, 0.000000000000000000, -1.000000000000000000 ) ) ;
#9546=ORIENTED_EDGE ( 'NONE', *, *, #18115, .F. ) ;
#9560=CARTESIAN_POINT ( 'NONE',  ( 10.36831320286038149, -3658.158799999850999, 2239.167815367355615 ) ) ;
#9582=VERTEX_POINT ( 'NONE', #7075 ) ;
#9590=AXIS2_PLACEMENT_3D ( 'NONE', #11534, #10012, #20341 ) ;
#9596=DIRECTION ( 'NONE',  ( 0.000000000000000000, 2.336881798971000105E-14, -1.000000000000000000 ) ) ;
#9607=ORIENTED_EDGE ( 'NONE', *, *, #8437, .F. ) ;
#9633=CARTESIAN_POINT ( 'NONE',  ( 15.03168679717000167, -3660.851200000000063, 2242.820000000000164 ) ) ;
#9660=LINE ( 'NONE', #16458, #11848 ) ;
#9692=ORIENTED_EDGE ( 'NONE', *, *, #6832, .T. ) ;
#9751=DIRECTION ( 'NONE',  ( 0.000000000000000000, 0.000000000000000000, 1.000000000000000000 ) ) ;
#9786=CYLINDRICAL_SURFACE ( 'NONE', #19815, 3.175000000000149925 ) ;
#9834=ORIENTED_EDGE ( 'NONE', *, *, #20468, .T. ) ;
#9844=DIRECTION ( 'NONE',  ( 0.000000000000000000, -2.336881798971000105E-14, 1.000000000000000000 ) ) ;
#9890=AXIS2_PLACEMENT_3D ( 'NONE', #2997, #22904, #6997 ) ;
#9918=CARTESIAN_POINT ( 'NONE',  ( 15.03168679717000167, -3660.851200000000063, 2239.391000000000076 ) ) ;
#10012=DIRECTION ( 'NONE',  ( -2.324635735433000053E-14, 2.336881798971000105E-14, -1.000000000000000000 ) ) ;
#10085=CYLINDRICAL_SURFACE ( 'NONE', #14416, 0.3810000000000260956 ) ;
#10089=ADVANCED_FACE ( 'NONE', ( #10896 ), #12769, .T. ) ;
#10196=EDGE_CURVE ( 'NONE', #12925, #13091, #11812, .T. ) ;
#10247=CARTESIAN_POINT ( 'NONE',  ( 12.69999999999999929, -3656.329999999999472, 2245.359999999999673 ) ) ;
#10294=ORIENTED_EDGE ( 'NONE', *, *, #10196, .F. ) ;
#10358=CARTESIAN_POINT ( 'NONE',  ( 12.69999999976724148, -3662.637340905157544, 2239.009999999999764 ) ) ;
#10412=VERTEX_POINT ( 'NONE', #8769 ) ;
#10417=ORIENTED_EDGE ( 'NONE', *, *, #10811, .F. ) ;
#10453=CARTESIAN_POINT ( 'NONE',  ( 12.69999999999999929, -3659.504999999999654, 2239.391000000000076 ) ) ;
#10495=EDGE_CURVE ( 'NONE', #3918, #20823, #3583, .T. ) ;
#10505=DIRECTION ( 'NONE',  ( 0.000000000000000000, -1.000000000000000000, 0.000000000000000000 ) ) ;
#10538=EDGE_CURVE ( 'NONE', #22029, #16601, #21918, .T. ) ;
#10638=VERTEX_POINT ( 'NONE', #12474 ) ;
#10710=AXIS2_PLACEMENT_3D ( 'NONE', #5327, #14123, #12472 ) ;
#10790=ORIENTED_EDGE ( 'NONE', *, *, #5525, .F. ) ;
#10800=CARTESIAN_POINT ( 'NONE',  ( 15.03168679716000078, -3658.158799999999701, 2242.820000000000164 ) ) ;
#10801=( NAMED_UNIT ( * ) SI_UNIT ( $, .STERADIAN. ) SOLID_ANGLE_UNIT ( ) );
#10811=EDGE_CURVE ( 'NONE', #424, #6944, #17071, .T. ) ;
#10893=EDGE_CURVE ( 'NONE', #9582, #15597, #15213, .T. ) ;
#10896=FACE_OUTER_BOUND ( 'NONE', #19048, .T. ) ;
#10946=EDGE_CURVE ( 'NONE', #12925, #15061, #7850, .T. ) ;
#10970=AXIS2_PLACEMENT_3D ( 'NONE', #10453, #13857, #6720 ) ;
#10987=CIRCLE ( 'NONE', #13980, 3.175000000000149925 ) ;
#11020=ORIENTED_EDGE ( 'NONE', *, *, #4278, .F. ) ;
#11045=AXIS2_PLACEMENT_3D ( 'NONE', #20110, #5819, #12950 ) ;
#11053=EDGE_LOOP ( 'NONE', ( #1441, #9692, #11935, #12236, #18984 ) ) ;
#11080=CARTESIAN_POINT ( 'NONE',  ( 12.69999999999999929, -3659.504999999999654, 2245.359999999999673 ) ) ;
#11081=VECTOR ( 'NONE', #9442, 1000.000000000000000 ) ;
#11122=ORIENTED_EDGE ( 'NONE', *, *, #6454, .T. ) ;
#11129=ORIENTED_EDGE ( 'NONE', *, *, #22315, .T. ) ;
#11165=DIRECTION ( 'NONE',  ( -2.324635735433000053E-14, 0.000000000000000000, -1.000000000000000000 ) ) ;
#11282=DIRECTION ( 'NONE',  ( 0.5000000000040877302, 0.8660254037820785955, 0.000000000000000000 ) ) ;
#11318=VECTOR ( 'NONE', #21066, 1000.000000000000000 ) ;
#11331=AXIS2_PLACEMENT_3D ( 'NONE', #430, #14731, #18346 ) ;
#11345=CARTESIAN_POINT ( 'NONE',  ( 12.69999999999999929, -3659.504999999999654, 2239.009999999999764 ) ) ;
#11379=EDGE_LOOP ( 'NONE', ( #18626, #18878, #14439, #20195, #4538 ) ) ;
#11384=FACE_OUTER_BOUND ( 'NONE', #22972, .T. ) ;
#11485=CARTESIAN_POINT ( 'NONE',  ( 10.36831320292846925, -3660.851200000039626, 2239.391000000000076 ) ) ;
#11513=SHAPE_DEFINITION_REPRESENTATION ( #9215, #16547 ) ;
#11534=CARTESIAN_POINT ( 'NONE',  ( 12.69999999999999929, -3659.504999999999654, 2239.009999999999764 ) ) ;
#11557=VERTEX_POINT ( 'NONE', #3810 ) ;
#11560=FACE_OUTER_BOUND ( 'NONE', #7063, .T. ) ;
#11563=ORIENTED_EDGE ( 'NONE', *, *, #21769, .F. ) ;
#11565=ORIENTED_EDGE ( 'NONE', *, *, #17290, .F. ) ;
#11585=ORIENTED_EDGE ( 'NONE', *, *, #9300, .F. ) ;
#11653=DIRECTION ( 'NONE',  ( 0.000000000000000000, 0.000000000000000000, -1.000000000000000000 ) ) ;
#11752=AXIS2_PLACEMENT_3D ( 'NONE', #8981, #7680, #20118 ) ;
#11791=DIRECTION ( 'NONE',  ( 0.000000000000000000, 0.000000000000000000, -1.000000000000000000 ) ) ;
#11812=LINE ( 'NONE', #19200, #2843 ) ;
#11846=VECTOR ( 'NONE', #15457, 999.9999999999998863 ) ;
#11848=VECTOR ( 'NONE', #6038, 1000.000000000000114 ) ;
#11893=CARTESIAN_POINT ( 'NONE',  ( 12.69999999999999929, -3659.504999999999654, 2239.391000000000076 ) ) ;
#11935=ORIENTED_EDGE ( 'NONE', *, *, #10893, .T. ) ;
#11972=PLANE ( 'NONE',  #20778 ) ;
#12017=PRODUCT_DEFINITION_FORMATION_WITH_SPECIFIED_SOURCE ( 'ANY', '', #3194, .NOT_KNOWN. ) ;
#12019=LINE ( 'NONE', #4517, #9346 ) ;
#12020=ORIENTED_EDGE ( 'NONE', *, *, #20569, .T. ) ;
#12045=DIRECTION ( 'NONE',  ( 0.000000000000000000, -1.000000000000000000, 0.000000000000000000 ) ) ;
#12092=ORIENTED_EDGE ( 'NONE', *, *, #20383, .T. ) ;
#12113=CARTESIAN_POINT ( 'NONE',  ( 12.70000000003999929, -3662.637340904999746, 2239.009999999999764 ) ) ;
#12141=EDGE_CURVE ( 'NONE', #16613, #11557, #13278, .T. ) ;
#12166=CIRCLE ( 'NONE', #1669, 1.904999999999823501 ) ;
#12201=ORIENTED_EDGE ( 'NONE', *, *, #13288, .T. ) ;
#12208=ORIENTED_EDGE ( 'NONE', *, *, #19906, .F. ) ;
#12210=DIRECTION ( 'NONE',  ( -2.324635735433000053E-14, 2.336881798971000105E-14, -1.000000000000000000 ) ) ;
#12232=ORIENTED_EDGE ( 'NONE', *, *, #20460, .T. ) ;
#12236=ORIENTED_EDGE ( 'NONE', *, *, #22315, .F. ) ;
#12286=ADVANCED_FACE ( 'NONE', ( #4189 ), #18368, .T. ) ;
#12298=DIRECTION ( 'NONE',  ( 0.000000000000000000, 0.000000000000000000, 1.000000000000000000 ) ) ;
#12309=CIRCLE ( 'NONE', #19046, 5.080000000000000959 ) ;
#12348=ORIENTED_EDGE ( 'NONE', *, *, #12530, .F. ) ;
#12405=ORIENTED_EDGE ( 'NONE', *, *, #21689, .F. ) ;
#12471=DIRECTION ( 'NONE',  ( -1.118034086297999961E-13, 2.590196616219000170E-13, -1.000000000000000000 ) ) ;
#12472=DIRECTION ( 'NONE',  ( 0.000000000000000000, -1.000000000000000000, 0.000000000000000000 ) ) ;
#12474=CARTESIAN_POINT ( 'NONE',  ( 12.69999999999999929, -3654.043999999999869, 2239.391000000000076 ) ) ;
#12501=CARTESIAN_POINT ( 'NONE',  ( 12.69999999999999929, -3659.504999999999654, 2270.760000000000218 ) ) ;
#12525=EDGE_LOOP ( 'NONE', ( #9434, #4968, #14755, #21981 ) ) ;
#12530=EDGE_CURVE ( 'NONE', #185, #13091, #22335, .T. ) ;
#12532=VECTOR ( 'NONE', #22076, 1000.000000000000114 ) ;
#12622=CARTESIAN_POINT ( 'NONE',  ( 15.18950216437265333, -3660.942314744880605, 2239.010000000072068 ) ) ;
#12733=DIRECTION ( 'NONE',  ( 0.000000000000000000, 1.000000000000000000, 0.000000000000000000 ) ) ;
#12769=CYLINDRICAL_SURFACE ( 'NONE', #5101, 0.3809999999999154618 ) ;
#12795=ADVANCED_FACE ( 'NONE', ( #2071 ), #9102, .T. ) ;
#12861=ORIENTED_EDGE ( 'NONE', *, *, #22453, .F. ) ;
#12864=TOROIDAL_SURFACE ( 'NONE', #19983, 1.905000000000000027, 1.270000000000000018 ) ;
#12910=FACE_OUTER_BOUND ( 'NONE', #22932, .T. ) ;
#12918=AXIS2_PLACEMENT_3D ( 'NONE', #14084, #2829, #5184 ) ;
#12925=VERTEX_POINT ( 'NONE', #984 ) ;
#12926=CARTESIAN_POINT ( 'NONE',  ( 12.69999999999999929, -3654.043999999999869, 2244.978999999999814 ) ) ;
#12934=AXIS2_PLACEMENT_3D ( 'NONE', #16951, #888, #6311 ) ;
#12950=DIRECTION ( 'NONE',  ( 1.000000000000000000, 5.432398939370943590E-28, -2.324635735433000369E-14 ) ) ;
#13003=UNCERTAINTY_MEASURE_WITH_UNIT (LENGTH_MEASURE( 1.000000000000000082E-05 ), #16076, 'distance_accuracy_value', 'NONE');
#13007=CARTESIAN_POINT ( 'NONE',  ( 12.69999999999999929, -3656.329999999999472, 2270.760000000000218 ) ) ;
#13012=CIRCLE ( 'NONE', #16369, 5.080000000000000071 ) ;
#13068=DIRECTION ( 'NONE',  ( 1.206643234470999950E-12, -1.000000000000000000, -2.336881798973999985E-14 ) ) ;
#13080=CARTESIAN_POINT ( 'NONE',  ( 7.619999999999999218, -3659.504999999999654, 2239.009999999999764 ) ) ;
#13091=VERTEX_POINT ( 'NONE', #1212 ) ;
#13092=CARTESIAN_POINT ( 'NONE',  ( 12.70000000002683471, -3656.630370510377816, 2239.010000000078435 ) ) ;
#13099=DIRECTION ( 'NONE',  ( 0.000000000000000000, 1.000000000000000000, 0.000000000000000000 ) ) ;
#13134=VERTEX_POINT ( 'NONE', #10358 ) ;
#13161=DIRECTION ( 'NONE',  ( 0.8660254037820785955, -0.5000000000040877302, -3.181634500919918361E-14 ) ) ;
#13169=EDGE_LOOP ( 'NONE', ( #6360, #21784, #6020, #16774, #4331 ) ) ;
#13175=ORIENTED_EDGE ( 'NONE', *, *, #10495, .T. ) ;
#13184=LINE ( 'NONE', #20454, #1220 ) ;
#13208=EDGE_CURVE ( 'NONE', #19866, #6944, #22993, .T. ) ;
#13245=ORIENTED_EDGE ( 'NONE', *, *, #20468, .F. ) ;
#13278=CIRCLE ( 'NONE', #8425, 1.904999999999823501 ) ;
#13288=EDGE_CURVE ( 'NONE', #17042, #18533, #14352, .T. ) ;
#13305=AXIS2_PLACEMENT_3D ( 'NONE', #9633, #16886, #16775 ) ;
#13319=CARTESIAN_POINT ( 'NONE',  ( 12.70000000028313281, -3656.372659094870869, 2239.009999999999764 ) ) ;
#13349=CARTESIAN_POINT ( 'NONE',  ( 12.70000000005999929, -3656.812599999999748, 2242.820000000000164 ) ) ;
#13362=ORIENTED_EDGE ( 'NONE', *, *, #20578, .T. ) ;
#13371=AXIS2_PLACEMENT_3D ( 'NONE', #7411, #9169, #376 ) ;
#13441=DIRECTION ( 'NONE',  ( 0.000000000000000000, 2.336881798971000105E-14, -1.000000000000000000 ) ) ;
#13462=DIRECTION ( 'NONE',  ( 0.000000000000000000, 0.000000000000000000, -1.000000000000000000 ) ) ;
#13474=DIRECTION ( 'NONE',  ( 5.572969907074833723E-14, -1.000000000000000000, 0.000000000000000000 ) ) ;
#13487=ORIENTED_EDGE ( 'NONE', *, *, #5525, .T. ) ;
#13502=CARTESIAN_POINT ( 'NONE',  ( 11.34365660143000021, -3661.854255679000289, 2239.391000000000076 ) ) ;
#13522=LINE ( 'NONE', #20659, #12532 ) ;
#13523=VERTEX_POINT ( 'NONE', #17240 ) ;
#13553=CARTESIAN_POINT ( 'NONE',  ( 12.69999999999999929, -3664.965999999999894, 2245.359999999999673 ) ) ;
#13561=LINE ( 'NONE', #22690, #6710 ) ;
#13571=CIRCLE ( 'NONE', #15814, 5.460999999999938126 ) ;
#13574=ADVANCED_FACE ( 'NONE', ( #8696, #15617 ), #11972, .F. ) ;
#13596=CLOSED_SHELL ( 'NONE', ( #5156, #22047, #8676, #4480, #2355, #21118, #13664, #6931, #7281, #976, #12795, #12286, #7585, #18965, #10089, #20536, #8416, #19291, #21827, #14620, #21461, #19087, #13574, #4973, #297, #21566 ) ) ;
#13614=CARTESIAN_POINT ( 'NONE',  ( 12.69999999976724148, -3662.637340905157544, 2239.009999999999764 ) ) ;
#13640=CARTESIAN_POINT ( 'NONE',  ( 12.70000000000017693, -3662.679999999999836, 2245.359999999999673 ) ) ;
#13664=ADVANCED_FACE ( 'NONE', ( #17831 ), #2013, .F. ) ;
#13668=CARTESIAN_POINT ( 'NONE',  ( 12.69999999999999929, -3659.504999999999654, 2244.978999999999814 ) ) ;
#13671=VECTOR ( 'NONE', #4424, 1000.000000000000000 ) ;
#13705=VECTOR ( 'NONE', #5333, 1000.000000000000000 ) ;
#13713=ORIENTED_EDGE ( 'NONE', *, *, #13208, .F. ) ;
#13774=DIRECTION ( 'NONE',  ( 0.000000000000000000, -1.000000000000000000, 0.000000000000000000 ) ) ;
#13782=VERTEX_POINT ( 'NONE', #21353 ) ;
#13789=EDGE_LOOP ( 'NONE', ( #21552, #11563, #2517, #4135 ) ) ;
#13796=CARTESIAN_POINT ( 'NONE',  ( 12.69999999999999929, -3659.504999999999654, 2272.030000000000200 ) ) ;
#13805=VERTEX_POINT ( 'NONE', #7173 ) ;
#13828=ORIENTED_EDGE ( 'NONE', *, *, #16650, .T. ) ;
#13857=DIRECTION ( 'NONE',  ( -2.324635735433000053E-14, 2.336881798971000105E-14, -1.000000000000000000 ) ) ;
#13877=DIRECTION ( 'NONE',  ( 0.000000000000000000, 0.000000000000000000, 1.000000000000000000 ) ) ;
#13898=ORIENTED_EDGE ( 'NONE', *, *, #20460, .F. ) ;
#13909=ORIENTED_EDGE ( 'NONE', *, *, #8136, .F. ) ;
#13949=ORIENTED_EDGE ( 'NONE', *, *, #18548, .F. ) ;
#13980=AXIS2_PLACEMENT_3D ( 'NONE', #8762, #18988, #13474 ) ;
#14084=CARTESIAN_POINT ( 'NONE',  ( 15.41268679717000012, -3659.504999999999654, 2239.391000000000076 ) ) ;
#14104=EDGE_CURVE ( 'NONE', #15061, #185, #13184, .T. ) ;
#14123=DIRECTION ( 'NONE',  ( 0.000000000000000000, 0.000000000000000000, -1.000000000000000000 ) ) ;
#14201=ORIENTED_EDGE ( 'NONE', *, *, #18115, .T. ) ;
#14208=ORIENTED_EDGE ( 'NONE', *, *, #21769, .T. ) ;
#14301=( BOUNDED_CURVE ( )  B_SPLINE_CURVE ( 3, ( #1535, #17584, #20760, #13614 ),
 .UNSPECIFIED., .F., .T. ) 
 B_SPLINE_CURVE_WITH_KNOTS ( ( 4, 4 ),
 ( 3.673835071120097305E-14, 1.570796326490076611 ),
 .UNSPECIFIED. ) 
 CURVE ( )  GEOMETRIC_REPRESENTATION_ITEM ( )  RATIONAL_B_SPLINE_CURVE ( ( 1.000000000000000000, 0.8047378541962203480, 0.8047378541962203480, 1.000000000000000000 ) ) 
 REPRESENTATION_ITEM ( '' )  );
#14352=LINE ( 'NONE', #19971, #909 ) ;
#14379=LINE ( 'NONE', #20119, #18189 ) ;
#14406=ORIENTED_EDGE ( 'NONE', *, *, #12141, .F. ) ;
#14416=AXIS2_PLACEMENT_3D ( 'NONE', #14941, #644, #7793 ) ;
#14439=ORIENTED_EDGE ( 'NONE', *, *, #16999, .T. ) ;
#14445=FACE_OUTER_BOUND ( 'NONE', #15058, .T. ) ;
#14506=ORIENTED_EDGE ( 'NONE', *, *, #14814, .F. ) ;
#14509=DIRECTION ( 'NONE',  ( 1.000000000000000000, 0.000000000000000000, 0.000000000000000000 ) ) ;
#14522=VECTOR ( 'NONE', #5493, 1000.000000000000000 ) ;
#14563=CARTESIAN_POINT ( 'NONE',  ( 10.36831320286361979, -3660.851200000155586, 2239.167815367206913 ) ) ;
#14603=( GEOMETRIC_REPRESENTATION_CONTEXT ( 3 ) GLOBAL_UNCERTAINTY_ASSIGNED_CONTEXT ( ( #13003 ) ) GLOBAL_UNIT_ASSIGNED_CONTEXT ( ( #16076, #1430, #10801 ) ) REPRESENTATION_CONTEXT ( 'NONE', 'WORKASPACE' ) );
#14620=ADVANCED_FACE ( 'NONE', ( #4949 ), #22180, .T. ) ;
#14731=DIRECTION ( 'NONE',  ( -2.324635735433000053E-14, 2.336881798971000105E-14, -1.000000000000000000 ) ) ;
#14755=ORIENTED_EDGE ( 'NONE', *, *, #15425, .T. ) ;
#14765=DIRECTION ( 'NONE',  ( -0.5000000000007065459, 0.8660254037840305896, 0.000000000000000000 ) ) ;
#14797=AXIS2_PLACEMENT_3D ( 'NONE', #2325, #7170, #13099 ) ;
#14814=EDGE_CURVE ( 'NONE', #13805, #16994, #2247, .T. ) ;
#14834=DIRECTION ( 'NONE',  ( 0.000000000000000000, 0.000000000000000000, -1.000000000000000000 ) ) ;
#14936=FACE_OUTER_BOUND ( 'NONE', #8782, .T. ) ;
#14941=CARTESIAN_POINT ( 'NONE',  ( 14.05634339859000015, -3661.854255679000289, 2239.391000000000076 ) ) ;
#15058=EDGE_LOOP ( 'NONE', ( #12348, #7135, #4023, #21991 ) ) ;
#15061=VERTEX_POINT ( 'NONE', #20260 ) ;
#15074=CIRCLE ( 'NONE', #4962, 3.175000000000149925 ) ;
#15191=CARTESIAN_POINT ( 'NONE',  ( 12.69999999999999929, -3659.504999999999654, 2270.760000000000218 ) ) ;
#15213=CIRCLE ( 'NONE', #3600, 0.3809999999999647002 ) ;
#15259=DIRECTION ( 'NONE',  ( -2.324635735433000053E-14, 0.000000000000000000, -1.000000000000000000 ) ) ;
#15279=CARTESIAN_POINT ( 'NONE',  ( 12.70000000003999929, -3662.197400000000016, 2242.820000000000164 ) ) ;
#15297=LINE ( 'NONE', #17273, #19972 ) ;
#15311=CARTESIAN_POINT ( 'NONE',  ( 12.70000000002640661, -3656.812599999840131, 2239.167815367326057 ) ) ;
#15315=DIRECTION ( 'NONE',  ( 2.324635735433000053E-14, 0.000000000000000000, 1.000000000000000000 ) ) ;
#15369=CARTESIAN_POINT ( 'NONE',  ( 12.69999999999999929, -3659.504999999999654, 2239.391000000000076 ) ) ;
#15425=EDGE_CURVE ( 'NONE', #13523, #16613, #19894, .T. ) ;
#15457=DIRECTION ( 'NONE',  ( 0.8660254037817188832, -0.5000000000047110094, -1.484475890921031808E-12 ) ) ;
#15487=CYLINDRICAL_SURFACE ( 'NONE', #12918, 0.3810000000000011156 ) ;
#15492=VECTOR ( 'NONE', #19903, 1000.000000000000000 ) ;
#15528=EDGE_LOOP ( 'NONE', ( #11020, #7343, #7099, #709 ) ) ;
#15537=ORIENTED_EDGE ( 'NONE', *, *, #10538, .F. ) ;
#15550=ORIENTED_EDGE ( 'NONE', *, *, #21194, .T. ) ;
#15582=DIRECTION ( 'NONE',  ( 0.000000000000000000, 1.000000000000000000, 0.000000000000000000 ) ) ;
#15597=VERTEX_POINT ( 'NONE', #13080 ) ;
#15617=FACE_OUTER_BOUND ( 'NONE', #8479, .T. ) ;
#15699=CIRCLE ( 'NONE', #22359, 1.269999999999882334 ) ;
#15777=CYLINDRICAL_SURFACE ( 'NONE', #9890, 0.3809999999999303388 ) ;
#15814=AXIS2_PLACEMENT_3D ( 'NONE', #21828, #11165, #2376 ) ;
#15863=EDGE_LOOP ( 'NONE', ( #18361, #4218, #8617, #4362 ) ) ;
#15867=DIRECTION ( 'NONE',  ( 0.000000000000000000, 1.000000000000000000, 0.000000000000000000 ) ) ;
#15978=EDGE_CURVE ( 'NONE', #16093, #20661, #22519, .T. ) ;
#15984=CARTESIAN_POINT ( 'NONE',  ( 7.238999999999998991, -3659.504999999999654, 2244.978999999999814 ) ) ;
#16069=EDGE_LOOP ( 'NONE', ( #13245, #12861, #9546, #12201 ) ) ;
#16076=( LENGTH_UNIT ( ) NAMED_UNIT ( * ) SI_UNIT ( .MILLI., .METRE. ) );
#16093=VERTEX_POINT ( 'NONE', #18896 ) ;
#16174=CARTESIAN_POINT ( 'NONE',  ( 10.36831320285999958, -3658.158799999999701, 2242.820000000000164 ) ) ;
#16245=CARTESIAN_POINT ( 'NONE',  ( 15.03168679710911704, -3660.851200000110111, 2239.391000000000076 ) ) ;
#16369=AXIS2_PLACEMENT_3D ( 'NONE', #603, #9844, #6120 ) ;
#16458=CARTESIAN_POINT ( 'NONE',  ( 15.41268679715999923, -3657.938829547000296, 2239.009999999999764 ) ) ;
#16474=CARTESIAN_POINT ( 'NONE',  ( 10.36831320293767078, -3658.158799999985604, 2239.391000000000076 ) ) ;
#16541=ORIENTED_EDGE ( 'NONE', *, *, #2300, .T. ) ;
#16547=SHAPE_REPRESENTATION ( 'Screw 4', ( #5611 ), #14603 ) ;
#16601=VERTEX_POINT ( 'NONE', #1849 ) ;
#16613=VERTEX_POINT ( 'NONE', #4064 ) ;
#16641=AXIS2_PLACEMENT_3D ( 'NONE', #9358, #4080, #1981 ) ;
#16650=EDGE_CURVE ( 'NONE', #13782, #9361, #23154, .T. ) ;
#16670=CARTESIAN_POINT ( 'NONE',  ( 12.69999999999999929, -3659.504999999999654, 2244.978999999999814 ) ) ;
#16702=FACE_BOUND ( 'NONE', #17951, .T. ) ;
#16741=UNCERTAINTY_MEASURE_WITH_UNIT (LENGTH_MEASURE( 1.000000000000000082E-05 ), #21126, 'distance_accuracy_value', 'NONE');
#16774=ORIENTED_EDGE ( 'NONE', *, *, #902, .T. ) ;
#16775=DIRECTION ( 'NONE',  ( -2.848935406719999894E-12, 1.000000000000000000, 0.000000000000000000 ) ) ;
#16802=CYLINDRICAL_SURFACE ( 'NONE', #17817, 0.3809999999999993947 ) ;
#16813=FACE_OUTER_BOUND ( 'NONE', #11053, .T. ) ;
#16886=DIRECTION ( 'NONE',  ( -1.000000000000000000, -2.848935406719999894E-12, 0.000000000000000000 ) ) ;
#16900=CARTESIAN_POINT ( 'NONE',  ( 9.987313202864001482, -3661.071170452999922, 2239.009999999999764 ) ) ;
#16939=CARTESIAN_POINT ( 'NONE',  ( 12.70000000002640839, -3656.812599999929262, 2239.391000000000076 ) ) ;
#16951=CARTESIAN_POINT ( 'NONE',  ( 12.69999999999999929, -3659.504999999999654, 2245.359999999999673 ) ) ;
#16963=DIRECTION ( 'NONE',  ( 0.000000000000000000, 0.000000000000000000, -1.000000000000000000 ) ) ;
#16994=VERTEX_POINT ( 'NONE', #66 ) ;
#16999=EDGE_CURVE ( 'NONE', #10638, #22029, #7582, .T. ) ;
#17042=VERTEX_POINT ( 'NONE', #15279 ) ;
#17071=CIRCLE ( 'NONE', #611, 5.460999999999938126 ) ;
#17078=CIRCLE ( 'NONE', #20452, 5.460999999999938126 ) ;
#17135=DIRECTION ( 'NONE',  ( -0.5000000000031962211, 0.8660254037825932949, 0.000000000000000000 ) ) ;
#17154=FACE_OUTER_BOUND ( 'NONE', #4819, .T. ) ;
#17240=CARTESIAN_POINT ( 'NONE',  ( 12.69999999999999929, -3656.329999999999472, 2270.760000000000218 ) ) ;
#17267=DIRECTION ( 'NONE',  ( 0.000000000000000000, 0.000000000000000000, 1.000000000000000000 ) ) ;
#17273=CARTESIAN_POINT ( 'NONE',  ( 12.70000000003999929, -3662.197400000000016, 2242.820000000000164 ) ) ;
#17290=EDGE_CURVE ( 'NONE', #9582, #10638, #13571, .T. ) ;
#17317=CARTESIAN_POINT ( 'NONE',  ( 12.70000000002425899, -3662.197400000083690, 2239.391000000000076 ) ) ;
#17548=LINE ( 'NONE', #443, #15492 ) ;
#17584=CARTESIAN_POINT ( 'NONE',  ( 12.70000000000865903, -3662.197400000167818, 2239.167815367317871 ) ) ;
#17599=DIRECTION ( 'NONE',  ( 0.000000000000000000, 0.000000000000000000, 1.000000000000000000 ) ) ;
#17609=ORIENTED_EDGE ( 'NONE', *, *, #7813, .F. ) ;
#17776=CARTESIAN_POINT ( 'NONE',  ( 15.41268679705191857, -3661.071170452636579, 2239.009999999999764 ) ) ;
#17781=CIRCLE ( 'NONE', #14797, 3.175000000000149925 ) ;
#17817=AXIS2_PLACEMENT_3D ( 'NONE', #7909, #13068, #20443 ) ;
#17824=DIRECTION ( 'NONE',  ( 0.000000000000000000, 1.000000000000000000, 0.000000000000000000 ) ) ;
#17831=FACE_OUTER_BOUND ( 'NONE', #23113, .T. ) ;
#17832=ORIENTED_EDGE ( 'NONE', *, *, #9300, .T. ) ;
#17898=LINE ( 'NONE', #5368, #14522 ) ;
#17937=DIRECTION ( 'NONE',  ( -2.903809793931999834E-13, 4.457650181899999573E-12, 1.000000000000000000 ) ) ;
#17951=EDGE_LOOP ( 'NONE', ( #20991, #11122, #19564, #20305, #23059, #12020 ) ) ;
#17998=CARTESIAN_POINT ( 'NONE',  ( 15.03168679717000167, -3660.851200000000063, 2242.820000000000164 ) ) ;
#18043=CARTESIAN_POINT ( 'NONE',  ( 11.34365660145000021, -3657.155744320999929, 2239.391000000000076 ) ) ;
#18082=ORIENTED_EDGE ( 'NONE', *, *, #13288, .F. ) ;
#18115=EDGE_CURVE ( 'NONE', #17042, #5087, #15297, .T. ) ;
#18189=VECTOR ( 'NONE', #5711, 1000.000000000000114 ) ;
#18201=ORIENTED_EDGE ( 'NONE', *, *, #9010, .F. ) ;
#18227=CIRCLE ( 'NONE', #2903, 3.175000000000149925 ) ;
#18280=EDGE_LOOP ( 'NONE', ( #7704, #8372, #17609, #3781 ) ) ;
#18285=CARTESIAN_POINT ( 'NONE',  ( 12.69999999999999929, -3664.965999999999894, 2244.978999999999814 ) ) ;
#18346=DIRECTION ( 'NONE',  ( 1.000000000000000000, 5.432398939370943590E-28, -2.324635735433000369E-14 ) ) ;
#18361=ORIENTED_EDGE ( 'NONE', *, *, #4837, .T. ) ;
#18368=PLANE ( 'NONE',  #16641 ) ;
#18384=LINE ( 'NONE', #13007, #8 ) ;
#18393=AXIS2_PLACEMENT_3D ( 'NONE', #5911, #11282, #4137 ) ;
#18533=VERTEX_POINT ( 'NONE', #17317 ) ;
#18548=EDGE_CURVE ( 'NONE', #5448, #5087, #17548, .T. ) ;
#18616=CARTESIAN_POINT ( 'NONE',  ( 12.69999999999999929, -3654.043999999999869, 2245.359999999999673 ) ) ;
#18626=ORIENTED_EDGE ( 'NONE', *, *, #10893, .F. ) ;
#18697=EDGE_CURVE ( 'NONE', #13805, #13091, #6090, .T. ) ;
#18706=CYLINDRICAL_SURFACE ( 'NONE', #12934, 5.460999999999938126 ) ;
#18811=DIRECTION ( 'NONE',  ( 0.000000000000000000, -1.000000000000000000, 0.000000000000000000 ) ) ;
#18842=CYLINDRICAL_SURFACE ( 'NONE', #6017, 5.460999999999938126 ) ;
#18868=ORIENTED_EDGE ( 'NONE', *, *, #2084, .T. ) ;
#18878=ORIENTED_EDGE ( 'NONE', *, *, #17290, .T. ) ;
#18896=CARTESIAN_POINT ( 'NONE',  ( 12.69999999999999929, -3662.679999999999836, 2270.760000000000218 ) ) ;
#18946=AXIS2_PLACEMENT_3D ( 'NONE', #20899, #17135, #19370 ) ;
#18965=ADVANCED_FACE ( 'NONE', ( #1469 ), #15777, .T. ) ;
#18984=ORIENTED_EDGE ( 'NONE', *, *, #7303, .F. ) ;
#18988=DIRECTION ( 'NONE',  ( 0.000000000000000000, 0.000000000000000000, -1.000000000000000000 ) ) ;
#19019=CARTESIAN_POINT ( 'NONE',  ( 17.78000000000000114, -3659.504999999999654, 2239.391000000000076 ) ) ;
#19032=CARTESIAN_POINT ( 'NONE',  ( 12.69999999999999929, -3659.504999999999654, 2272.030000000000200 ) ) ;
#19046=AXIS2_PLACEMENT_3D ( 'NONE', #6313, #13441, #20581 ) ;
#19048=EDGE_LOOP ( 'NONE', ( #19912, #16541, #14506, #5749 ) ) ;
#19073=EDGE_LOOP ( 'NONE', ( #19818, #10294, #10790, #17832 ) ) ;
#19087=ADVANCED_FACE ( 'NONE', ( #9327 ), #20039, .T. ) ;
#19095=VERTEX_POINT ( 'NONE', #187 ) ;
#19151=CARTESIAN_POINT ( 'NONE',  ( 15.03168679710911704, -3660.851200000110111, 2239.391000000000076 ) ) ;
#19200=CARTESIAN_POINT ( 'NONE',  ( 12.70000000005999929, -3656.812599999999748, 2242.820000000000164 ) ) ;
#19279=LINE ( 'NONE', #5222, #13705 ) ;
#19291=ADVANCED_FACE ( 'NONE', ( #20331 ), #10085, .T. ) ;
#19302=ORIENTED_EDGE ( 'NONE', *, *, #8781, .T. ) ;
#19340=ORIENTED_EDGE ( 'NONE', *, *, #14104, .T. ) ;
#19347=VECTOR ( 'NONE', #845, 1000.000000000000000 ) ;
#19370=DIRECTION ( 'NONE',  ( 0.000000000000000000, 0.000000000000000000, 1.000000000000000000 ) ) ;
#19478=SHAPE_REPRESENTATION_RELATIONSHIP ( 'NONE' , 'NONE' ,  #16547, #2374 ) ;
#19549=EDGE_CURVE ( 'NONE', #3918, #19866, #19644, .T. ) ;
#19557=CARTESIAN_POINT ( 'NONE',  ( 15.03168679717000167, -3660.851200000000063, 2239.391000000000076 ) ) ;
#19564=ORIENTED_EDGE ( 'NONE', *, *, #14814, .T. ) ;
#19631=CARTESIAN_POINT ( 'NONE',  ( 10.36831320285999958, -3660.851200000000063, 2242.820000000000164 ) ) ;
#19644=CIRCLE ( 'NONE', #9536, 5.080000000000000071 ) ;
#19645=PLANE ( 'NONE',  #6588 ) ;
#19651=DIRECTION ( 'NONE',  ( 0.000000000000000000, 0.000000000000000000, 1.000000000000000000 ) ) ;
#19703=VECTOR ( 'NONE', #6736, 1000.000000000000114 ) ;
#19781=CARTESIAN_POINT ( 'NONE',  ( 12.69999999999999929, -3657.599999999999909, 2270.760000000000218 ) ) ;
#19815=AXIS2_PLACEMENT_3D ( 'NONE', #15191, #11653, #18811 ) ;
#19818=ORIENTED_EDGE ( 'NONE', *, *, #8570, .F. ) ;
#19866=VERTEX_POINT ( 'NONE', #5384 ) ;
#19894=CIRCLE ( 'NONE', #3421, 1.269999999999882334 ) ;
#19903=DIRECTION ( 'NONE',  ( 7.280632624814000430E-13, -1.000000000000000000, 4.288485907146999317E-12 ) ) ;
#19906=EDGE_CURVE ( 'NONE', #796, #21944, #22714, .T. ) ;
#19912=ORIENTED_EDGE ( 'NONE', *, *, #8570, .T. ) ;
#19947=CARTESIAN_POINT ( 'NONE',  ( 12.70000000005999929, -3656.372659094999563, 2239.009999999999764 ) ) ;
#19971=CARTESIAN_POINT ( 'NONE',  ( 12.70000000003999929, -3662.197400000000016, 2242.820000000000164 ) ) ;
#19972=VECTOR ( 'NONE', #8382, 1000.000000000000000 ) ;
#19983=AXIS2_PLACEMENT_3D ( 'NONE', #7507, #21584, #17824 ) ;
#20022=ORIENTED_EDGE ( 'NONE', *, *, #19906, .T. ) ;
#20039=TOROIDAL_SURFACE ( 'NONE', #11045, 5.080000000000000071, 0.3810000000000000053 ) ;
#20058=EDGE_CURVE ( 'NONE', #424, #16601, #7478, .T. ) ;
#20110=CARTESIAN_POINT ( 'NONE',  ( 12.69999999999999929, -3659.504999999999654, 2244.978999999999814 ) ) ;
#20111=DIRECTION ( 'NONE',  ( 5.572969907074833723E-14, -1.000000000000000000, 0.000000000000000000 ) ) ;
#20118=DIRECTION ( 'NONE',  ( -1.206643234470999950E-12, 1.000000000000000000, 0.000000000000000000 ) ) ;
#20119=CARTESIAN_POINT ( 'NONE',  ( 12.70000000003999929, -3662.197400000000016, 2239.391000000000076 ) ) ;
#20195=ORIENTED_EDGE ( 'NONE', *, *, #7303, .T. ) ;
#20219=CARTESIAN_POINT ( 'NONE',  ( 12.69999999999999929, -3659.504999999999654, 2244.978999999999814 ) ) ;
#20260=CARTESIAN_POINT ( 'NONE',  ( 15.03168679716000078, -3658.158799999999701, 2242.820000000000164 ) ) ;
#20305=ORIENTED_EDGE ( 'NONE', *, *, #22408, .F. ) ;
#20331=FACE_OUTER_BOUND ( 'NONE', #13789, .T. ) ;
#20335=DIRECTION ( 'NONE',  ( 0.000000000000000000, -1.000000000000000000, 0.000000000000000000 ) ) ;
#20341=DIRECTION ( 'NONE',  ( -1.000000000000000000, 0.000000000000000000, 2.324635735433000053E-14 ) ) ;
#20364=EDGE_LOOP ( 'NONE', ( #5247, #11585, #4888, #21122 ) ) ;
#20383=EDGE_CURVE ( 'NONE', #21944, #17042, #5594, .T. ) ;
#20387=ORIENTED_EDGE ( 'NONE', *, *, #6832, .F. ) ;
#20443=DIRECTION ( 'NONE',  ( -1.000000000000000000, -1.165588477296754225E-12, 0.000000000000000000 ) ) ;
#20452=AXIS2_PLACEMENT_3D ( 'NONE', #13668, #15315, #20818 ) ;
#20454=CARTESIAN_POINT ( 'NONE',  ( 15.03168679716000078, -3658.158799999999701, 2242.820000000000164 ) ) ;
#20460=EDGE_CURVE ( 'NONE', #20823, #424, #3581, .T. ) ;
#20468=EDGE_CURVE ( 'NONE', #2777, #18533, #13522, .T. ) ;
#20518=PLANE ( 'NONE',  #13305 ) ;
#20536=ADVANCED_FACE ( 'NONE', ( #2519 ), #16802, .T. ) ;
#20569=EDGE_CURVE ( 'NONE', #13134, #9361, #5207, .T. ) ;
#20578=EDGE_CURVE ( 'NONE', #11557, #16613, #12166, .T. ) ;
#20581=DIRECTION ( 'NONE',  ( 1.000000000000000000, 0.000000000000000000, 0.000000000000000000 ) ) ;
#20652=ORIENTED_EDGE ( 'NONE', *, *, #4293, .T. ) ;
#20659=CARTESIAN_POINT ( 'NONE',  ( 10.36831320285999958, -3660.851200000000063, 2239.391000000000076 ) ) ;
#20661=VERTEX_POINT ( 'NONE', #13640 ) ;
#20678=EDGE_LOOP ( 'NONE', ( #8813, #4202 ) ) ;
#20760=CARTESIAN_POINT ( 'NONE',  ( 12.70000000000855955, -3662.379629489641502, 2239.010000000067976 ) ) ;
#20778=AXIS2_PLACEMENT_3D ( 'NONE', #1539, #12210, #4711 ) ;
#20781=VERTEX_POINT ( 'NONE', #12926 ) ;
#20793=DIRECTION ( 'NONE',  ( 1.224646799141920914E-16, -1.000000000000000000, -2.336881798971000421E-14 ) ) ;
#20818=DIRECTION ( 'NONE',  ( 0.000000000000000000, -1.000000000000000000, 0.000000000000000000 ) ) ;
#20823=VERTEX_POINT ( 'NONE', #15984 ) ;
#20899=CARTESIAN_POINT ( 'NONE',  ( 12.70000000003999929, -3662.197400000000016, 2242.820000000000164 ) ) ;
#20900=CARTESIAN_POINT ( 'NONE',  ( 12.69999999999999929, -3662.679999999999836, 2270.760000000000218 ) ) ;
#20943=DIRECTION ( 'NONE',  ( -1.103190638852999933E-12, 1.000000000000000000, 0.000000000000000000 ) ) ;
#20962=PRODUCT_DEFINITION ( 'UNKNOWN', '', #12017, #5972 ) ;
#20991=ORIENTED_EDGE ( 'NONE', *, *, #16650, .F. ) ;
#21053=EDGE_CURVE ( 'NONE', #18533, #13134, #14301, .T. ) ;
#21066=DIRECTION ( 'NONE',  ( -2.807875838775999975E-12, 1.000000000000000000, 0.000000000000000000 ) ) ;
#21075=DIRECTION ( 'NONE',  ( -2.580078660703000173E-14, 3.885294924352999876E-13, -1.000000000000000000 ) ) ;
#21118=ADVANCED_FACE ( 'NONE', ( #3175 ), #15487, .T. ) ;
#21122=ORIENTED_EDGE ( 'NONE', *, *, #22453, .T. ) ;
#21126=( LENGTH_UNIT ( ) NAMED_UNIT ( * ) SI_UNIT ( .MILLI., .METRE. ) );
#21184=DIRECTION ( 'NONE',  ( 0.000000000000000000, 0.000000000000000000, -1.000000000000000000 ) ) ;
#21194=EDGE_CURVE ( 'NONE', #13523, #16093, #17781, .T. ) ;
#21208=MANIFOLD_SOLID_BREP ( 'TORNILLO3[1]', #13596 ) ;
#21235=CARTESIAN_POINT ( 'NONE',  ( 15.03168679710029743, -3658.158799999889197, 2239.391000000000076 ) ) ;
#21268=CARTESIAN_POINT ( 'NONE',  ( 18.16100000000000136, -3659.504999999999654, 2239.391000000000076 ) ) ;
#21353=CARTESIAN_POINT ( 'NONE',  ( 15.41268679728733915, -3657.938829547220848, 2239.009999999999764 ) ) ;
#21381=FACE_OUTER_BOUND ( 'NONE', #18280, .T. ) ;
#21436=CARTESIAN_POINT ( 'NONE',  ( 12.69999999999999929, -3659.504999999999654, 2272.030000000000200 ) ) ;
#21461=ADVANCED_FACE ( 'NONE', ( #11560 ), #18706, .T. ) ;
#21552=ORIENTED_EDGE ( 'NONE', *, *, #21689, .T. ) ;
#21566=ADVANCED_FACE ( 'NONE', ( #3589 ), #19645, .F. ) ;
#21584=DIRECTION ( 'NONE',  ( 0.000000000000000000, 0.000000000000000000, 1.000000000000000000 ) ) ;
#21588=CARTESIAN_POINT ( 'NONE',  ( 15.03168679716000078, -3655.466399999999794, 2242.820000000000164 ) ) ;
#21649=ORIENTED_EDGE ( 'NONE', *, *, #4293, .F. ) ;
#21662=VECTOR ( 'NONE', #3007, 1000.000000000000000 ) ;
#21689=EDGE_CURVE ( 'NONE', #18533, #796, #14379, .T. ) ;
#21769=EDGE_CURVE ( 'NONE', #9361, #796, #4705, .T. ) ;
#21784=ORIENTED_EDGE ( 'NONE', *, *, #8781, .F. ) ;
#21827=ADVANCED_FACE ( 'NONE', ( #16702, #17154 ), #22082, .T. ) ;
#21828=CARTESIAN_POINT ( 'NONE',  ( 12.69999999999999929, -3659.504999999999654, 2239.391000000000076 ) ) ;
#21906=LINE ( 'NONE', #18616, #6366 ) ;
#21918=CIRCLE ( 'NONE', #7724, 5.460999999999938126 ) ;
#21937=ORIENTED_EDGE ( 'NONE', *, *, #10811, .T. ) ;
#21944=VERTEX_POINT ( 'NONE', #1570 ) ;
#21945=PLANE ( 'NONE',  #18393 ) ;
#21959=DIRECTION ( 'NONE',  ( 0.000000000000000000, 0.000000000000000000, 1.000000000000000000 ) ) ;
#21979=CARTESIAN_POINT ( 'NONE',  ( 9.987313202991684236, -3657.938829547518253, 2239.009999999999764 ) ) ;
#21981=ORIENTED_EDGE ( 'NONE', *, *, #20578, .F. ) ;
#21991=ORIENTED_EDGE ( 'NONE', *, *, #10196, .T. ) ;
#22029=VERTEX_POINT ( 'NONE', #21268 ) ;
#22047=ADVANCED_FACE ( 'NONE', ( #21381 ), #6632, .T. ) ;
#22061=FACE_OUTER_BOUND ( 'NONE', #4891, .T. ) ;
#22076=DIRECTION ( 'NONE',  ( 0.8660254037820102058, -0.5000000000042060799, 0.000000000000000000 ) ) ;
#22082=PLANE ( 'NONE',  #9590 ) ;
#22162=ORIENTED_EDGE ( 'NONE', *, *, #18697, .F. ) ;
#22180=TOROIDAL_SURFACE ( 'NONE', #10970, 5.080000000000000071, 0.3810000000000000053 ) ;
#22266=VECTOR ( 'NONE', #6909, 1000.000000000000000 ) ;
#22278=DIRECTION ( 'NONE',  ( 2.324635735433000053E-14, 0.000000000000000000, 1.000000000000000000 ) ) ;
#22315=EDGE_CURVE ( 'NONE', #9475, #15597, #12309, .T. ) ;
#22335=LINE ( 'NONE', #2893, #13671 ) ;
#22359=AXIS2_PLACEMENT_3D ( 'NONE', #9206, #303, #1937 ) ;
#22408=EDGE_CURVE ( 'NONE', #19095, #16994, #13561, .T. ) ;
#22453=EDGE_CURVE ( 'NONE', #5087, #2777, #5009, .T. ) ;
#22498=DIRECTION ( 'NONE',  ( 0.000000000000000000, -1.000000000000000000, 0.000000000000000000 ) ) ;
#22519=LINE ( 'NONE', #20900, #1182 ) ;
#22535=CARTESIAN_POINT ( 'NONE',  ( 17.78000000000000114, -3659.504999999999654, 2244.978999999999814 ) ) ;
#22541=DIRECTION ( 'NONE',  ( -3.308571459023000057E-13, 2.590196616237999979E-13, -1.000000000000000000 ) ) ;
#22655=AXIS2_PLACEMENT_3D ( 'NONE', #20219, #1090, #20335 ) ;
#22657=ORIENTED_EDGE ( 'NONE', *, *, #9010, .T. ) ;
#22690=CARTESIAN_POINT ( 'NONE',  ( 9.987313202864001482, -3661.071170452999922, 2239.009999999999764 ) ) ;
#22714=LINE ( 'NONE', #19557, #22266 ) ;
#22756=DIRECTION ( 'NONE',  ( 0.000000000000000000, 0.000000000000000000, -1.000000000000000000 ) ) ;
#22784=ORIENTED_EDGE ( 'NONE', *, *, #902, .F. ) ;
#22904=DIRECTION ( 'NONE',  ( -0.8660254037817188832, 0.5000000000047110094, 3.181634500920069822E-14 ) ) ;
#22915=CARTESIAN_POINT ( 'NONE',  ( 10.36831320285999958, -3660.851200000000063, 2242.820000000000164 ) ) ;
#22932=EDGE_LOOP ( 'NONE', ( #8283, #13175, #12232, #21937, #13713 ) ) ;
#22972=EDGE_LOOP ( 'NONE', ( #3664, #20022, #3551, #19340 ) ) ;
#22993=CIRCLE ( 'NONE', #6173, 0.3809999999999647002 ) ;
#23059=ORIENTED_EDGE ( 'NONE', *, *, #8437, .T. ) ;
#23094=( NAMED_UNIT ( * ) SI_UNIT ( $, .STERADIAN. ) SOLID_ANGLE_UNIT ( ) );
#23113=EDGE_LOOP ( 'NONE', ( #12092, #14201, #13949, #13487, #9179, #13909 ) ) ;
#23154=LINE ( 'NONE', #2312, #6453 ) ;
#23208=COLOUR_RGB('Black',0.12,0.14,0.17);
#23209=FILL_AREA_STYLE_COLOUR('',#23208);
#23210=FILL_AREA_STYLE('',(#23209));
#23211=SURFACE_STYLE_FILL_AREA(#23210);
#23212=SURFACE_SIDE_STYLE('',(#23211));
#23213=SURFACE_STYLE_USAGE(.BOTH.,#23212);
#23214=PRESENTATION_STYLE_ASSIGNMENT((#23213));
#23233=STYLED_ITEM('',(#23214),#21208);
#23237=MECHANICAL_DESIGN_GEOMETRIC_PRESENTATION_REPRESENTATION('',(#23233),#2257);
ENDSEC;
END-ISO-10303-21;
